ISO-10303-21;
HEADER;
/* Generated by software containing ST-Developer
 * from STEP Tools, Inc. (www.steptools.com) 
 */

FILE_DESCRIPTION(
/* description */ ('Double-row support with tensioned shaft'),
/* implementation_level */ '2;1');

FILE_NAME(
/* name */ 'Bonded foot pad (3).step',
/* time_stamp */ '2026-10-27T10:50:35-07:00',
/* author */ (''),
/* organization */ (''),
/* preprocessor_version */ 'ST-DEVELOPER v20.2',
/* originating_system */ 'Autodesk Translation Framework v15.17.0.0',
/* authorisation */ '');

FILE_SCHEMA (('AUTOMOTIVE_DESIGN { 1 0 10303 214 3 1 1 }'));
ENDSEC;

DATA;
#10=MECHANICAL_DESIGN_GEOMETRIC_PRESENTATION_REPRESENTATION('',(#483),#11559);
#419=SHAPE_REPRESENTATION_RELATIONSHIP('SRR','None',#11727,#451);
#451=ADVANCED_BREP_SHAPE_REPRESENTATION('',(#516),#11529);
#483=STYLED_ITEM('',(#11960),#516);
#516=MANIFOLD_SOLID_BREP('Body1',#6328);
#703=PLANE('',#6780);
#704=PLANE('',#6781);
#705=PLANE('',#6782);
#706=PLANE('',#6783);
#707=PLANE('',#6784);
#708=PLANE('',#6785);
#953=FACE_OUTER_BOUND('',#1321,.T.);
#954=FACE_OUTER_BOUND('',#1322,.T.);
#955=FACE_OUTER_BOUND('',#1323,.T.);
#956=FACE_OUTER_BOUND('',#1324,.T.);
#957=FACE_OUTER_BOUND('',#1325,.T.);
#958=FACE_OUTER_BOUND('',#1326,.T.);
#1321=EDGE_LOOP('',(#4498,#4499,#4500,#4501));
#1322=EDGE_LOOP('',(#4502,#4503,#4504,#4505));
#1323=EDGE_LOOP('',(#4506,#4507,#4508,#4509));
#1324=EDGE_LOOP('',(#4510,#4511,#4512,#4513));
#1325=EDGE_LOOP('',(#4514,#4515,#4516,#4517));
#1326=EDGE_LOOP('',(#4518,#4519,#4520,#4521));
#1802=LINE('',#9420,#2349);
#1803=LINE('',#9422,#2350);
#1804=LINE('',#9424,#2351);
#1805=LINE('',#9425,#2352);
#1806=LINE('',#9428,#2353);
#1807=LINE('',#9430,#2354);
#1808=LINE('',#9431,#2355);
#1809=LINE('',#9434,#2356);
#1810=LINE('',#9436,#2357);
#1811=LINE('',#9437,#2358);
#1812=LINE('',#9439,#2359);
#1813=LINE('',#9440,#2360);
#2349=VECTOR('',#7567,1.);
#2350=VECTOR('',#7568,1.);
#2351=VECTOR('',#7569,1.);
#2352=VECTOR('',#7570,1.);
#2353=VECTOR('',#7573,1.);
#2354=VECTOR('',#7574,1.);
#2355=VECTOR('',#7575,1.);
#2356=VECTOR('',#7578,1.);
#2357=VECTOR('',#7579,1.);
#2358=VECTOR('',#7580,1.);
#2359=VECTOR('',#7583,1.);
#2360=VECTOR('',#7584,1.);
#3083=VERTEX_POINT('',#9418);
#3084=VERTEX_POINT('',#9419);
#3085=VERTEX_POINT('',#9421);
#3086=VERTEX_POINT('',#9423);
#3087=VERTEX_POINT('',#9427);
#3088=VERTEX_POINT('',#9429);
#3089=VERTEX_POINT('',#9433);
#3090=VERTEX_POINT('',#9435);
#3634=EDGE_CURVE('',#3083,#3084,#1802,.T.);
#3635=EDGE_CURVE('',#3084,#3085,#1803,.T.);
#3636=EDGE_CURVE('',#3086,#3085,#1804,.T.);
#3637=EDGE_CURVE('',#3083,#3086,#1805,.T.);
#3638=EDGE_CURVE('',#3087,#3083,#1806,.T.);
#3639=EDGE_CURVE('',#3088,#3086,#1807,.T.);
#3640=EDGE_CURVE('',#3087,#3088,#1808,.T.);
#3641=EDGE_CURVE('',#3089,#3087,#1809,.T.);
#3642=EDGE_CURVE('',#3090,#3088,#1810,.T.);
#3643=EDGE_CURVE('',#3089,#3090,#1811,.T.);
#3644=EDGE_CURVE('',#3084,#3089,#1812,.T.);
#3645=EDGE_CURVE('',#3085,#3090,#1813,.T.);
#4498=ORIENTED_EDGE('',*,*,#3634,.T.);
#4499=ORIENTED_EDGE('',*,*,#3635,.T.);
#4500=ORIENTED_EDGE('',*,*,#3636,.F.);
#4501=ORIENTED_EDGE('',*,*,#3637,.F.);
#4502=ORIENTED_EDGE('',*,*,#3638,.T.);
#4503=ORIENTED_EDGE('',*,*,#3637,.T.);
#4504=ORIENTED_EDGE('',*,*,#3639,.F.);
#4505=ORIENTED_EDGE('',*,*,#3640,.F.);
#4506=ORIENTED_EDGE('',*,*,#3641,.T.);
#4507=ORIENTED_EDGE('',*,*,#3640,.T.);
#4508=ORIENTED_EDGE('',*,*,#3642,.F.);
#4509=ORIENTED_EDGE('',*,*,#3643,.F.);
#4510=ORIENTED_EDGE('',*,*,#3644,.T.);
#4511=ORIENTED_EDGE('',*,*,#3643,.T.);
#4512=ORIENTED_EDGE('',*,*,#3645,.F.);
#4513=ORIENTED_EDGE('',*,*,#3635,.F.);
#4514=ORIENTED_EDGE('',*,*,#3645,.T.);
#4515=ORIENTED_EDGE('',*,*,#3642,.T.);
#4516=ORIENTED_EDGE('',*,*,#3639,.T.);
#4517=ORIENTED_EDGE('',*,*,#3636,.T.);
#4518=ORIENTED_EDGE('',*,*,#3644,.F.);
#4519=ORIENTED_EDGE('',*,*,#3634,.F.);
#4520=ORIENTED_EDGE('',*,*,#3638,.F.);
#4521=ORIENTED_EDGE('',*,*,#3641,.F.);
#6016=ADVANCED_FACE('',(#953),#703,.T.);
#6017=ADVANCED_FACE('',(#954),#704,.T.);
#6018=ADVANCED_FACE('',(#955),#705,.T.);
#6019=ADVANCED_FACE('',(#956),#706,.T.);
#6020=ADVANCED_FACE('',(#957),#707,.T.);
#6021=ADVANCED_FACE('',(#958),#708,.F.);
#6328=CLOSED_SHELL('',(#6016,#6017,#6018,#6019,#6020,#6021));
#6779=AXIS2_PLACEMENT_3D('',#9416,#7563,#7564);
#6780=AXIS2_PLACEMENT_3D('',#9417,#7565,#7566);
#6781=AXIS2_PLACEMENT_3D('',#9426,#7571,#7572);
#6782=AXIS2_PLACEMENT_3D('',#9432,#7576,#7577);
#6783=AXIS2_PLACEMENT_3D('',#9438,#7581,#7582);
#6784=AXIS2_PLACEMENT_3D('',#9441,#7585,#7586);
#6785=AXIS2_PLACEMENT_3D('',#9442,#7587,#7588);
#7563=DIRECTION('axis',(0.,0.,1.));
#7564=DIRECTION('refdir',(1.,0.,0.));
#7565=DIRECTION('center_axis',(0.,1.,0.));
#7566=DIRECTION('ref_axis',(-1.,0.,0.));
#7567=DIRECTION('',(-1.,0.,0.));
#7568=DIRECTION('',(0.,0.,1.));
#7569=DIRECTION('',(-1.,0.,0.));
#7570=DIRECTION('',(0.,0.,1.));
#7571=DIRECTION('center_axis',(1.,0.,0.));
#7572=DIRECTION('ref_axis',(0.,1.,0.));
#7573=DIRECTION('',(0.,1.,0.));
#7574=DIRECTION('',(0.,1.,0.));
#7575=DIRECTION('',(0.,0.,1.));
#7576=DIRECTION('center_axis',(0.,-1.,0.));
#7577=DIRECTION('ref_axis',(1.,0.,0.));
#7578=DIRECTION('',(1.,0.,0.));
#7579=DIRECTION('',(1.,0.,0.));
#7580=DIRECTION('',(0.,0.,1.));
#7581=DIRECTION('center_axis',(-1.,0.,0.));
#7582=DIRECTION('ref_axis',(0.,-1.,0.));
#7583=DIRECTION('',(0.,-1.,0.));
#7584=DIRECTION('',(0.,-1.,0.));
#7585=DIRECTION('center_axis',(0.,0.,1.));
#7586=DIRECTION('ref_axis',(1.,0.,0.));
#7587=DIRECTION('center_axis',(0.,0.,1.));
#7588=DIRECTION('ref_axis',(1.,0.,0.));
#9416=CARTESIAN_POINT('',(0.,0.,0.));
#9417=CARTESIAN_POINT('Origin',(10.,22.,-0.4));
#9418=CARTESIAN_POINT('',(10.,22.,-0.4));
#9419=CARTESIAN_POINT('',(-10.,22.,-0.4));
#9420=CARTESIAN_POINT('',(10.,22.,-0.4));
#9421=CARTESIAN_POINT('',(-10.,22.,0.));
#9422=CARTESIAN_POINT('',(-10.,22.,-0.4));
#9423=CARTESIAN_POINT('',(10.,22.,0.));
#9424=CARTESIAN_POINT('',(10.,22.,0.));
#9425=CARTESIAN_POINT('',(10.,22.,-0.4));
#9426=CARTESIAN_POINT('Origin',(10.,20.,-0.4));
#9427=CARTESIAN_POINT('',(10.,20.,-0.4));
#9428=CARTESIAN_POINT('',(10.,20.,-0.4));
#9429=CARTESIAN_POINT('',(10.,20.,0.));
#9430=CARTESIAN_POINT('',(10.,20.,0.));
#9431=CARTESIAN_POINT('',(10.,20.,-0.4));
#9432=CARTESIAN_POINT('Origin',(-10.,20.,-0.4));
#9433=CARTESIAN_POINT('',(-10.,20.,-0.4));
#9434=CARTESIAN_POINT('',(-10.,20.,-0.4));
#9435=CARTESIAN_POINT('',(-10.,20.,0.));
#9436=CARTESIAN_POINT('',(-10.,20.,0.));
#9437=CARTESIAN_POINT('',(-10.,20.,-0.4));
#9438=CARTESIAN_POINT('Origin',(-10.,22.,-0.4));
#9439=CARTESIAN_POINT('',(-10.,22.,-0.4));
#9440=CARTESIAN_POINT('',(-10.,22.,0.));
#9441=CARTESIAN_POINT('Origin',(0.,21.,0.));
#9442=CARTESIAN_POINT('Origin',(0.,21.,-0.4));
#11492=UNCERTAINTY_MEASURE_WITH_UNIT(LENGTH_MEASURE(0.001),#11560,
'DISTANCE_ACCURACY_VALUE',
'Maximum model space distance between geometric entities at asserted c
onnectivities');
#11522=UNCERTAINTY_MEASURE_WITH_UNIT(LENGTH_MEASURE(0.001),#11560,
'DISTANCE_ACCURACY_VALUE',
'Maximum model space distance between geometric entities at asserted c
onnectivities');
#11529=(
GEOMETRIC_REPRESENTATION_CONTEXT(3)
GLOBAL_UNCERTAINTY_ASSIGNED_CONTEXT((#11492))
GLOBAL_UNIT_ASSIGNED_CONTEXT((#11560,#11562,#11563))
REPRESENTATION_CONTEXT('','3D')
);
#11559=(
GEOMETRIC_REPRESENTATION_CONTEXT(3)
GLOBAL_UNCERTAINTY_ASSIGNED_CONTEXT((#11522))
GLOBAL_UNIT_ASSIGNED_CONTEXT((#11560,#11562,#11563))
REPRESENTATION_CONTEXT('','3D')
);
#11560=(
LENGTH_UNIT()
NAMED_UNIT(*)
SI_UNIT(.CENTI.,.METRE.)
);
#11562=(
NAMED_UNIT(*)
PLANE_ANGLE_UNIT()
SI_UNIT($,.RADIAN.)
);
#11563=(
NAMED_UNIT(*)
SI_UNIT($,.STERADIAN.)
SOLID_ANGLE_UNIT()
);
#11570=SHAPE_DEFINITION_REPRESENTATION(#11606,#11727);
#11606=PRODUCT_DEFINITION_SHAPE('',$,#11764);
#11727=SHAPE_REPRESENTATION('',(#6779),#11529);
#11757=PRODUCT_DEFINITION_CONTEXT('part definition',#11867,'design');
#11764=PRODUCT_DEFINITION('Bonded foot pad (3)','Bonded foot pad (3)',#11800,
#11757);
#11800=PRODUCT_DEFINITION_FORMATION('',$,#11875);
#11867=APPLICATION_CONTEXT(
'Core Data for Automotive Mechanical Design Process');
#11868=PRODUCT_CONTEXT('part definition',#11867,'mechanical');
#11875=PRODUCT('Bonded foot pad (3)','Bonded foot pad (3)',
'Bonded foot pad (3)',(#11868));
#11954=COLOUR_RGB('Sky Blue',0.24,0.69,0.87);
#11955=FILL_AREA_STYLE_COLOUR('',#11954);
#11956=FILL_AREA_STYLE('',(#11955));
#11957=SURFACE_STYLE_FILL_AREA(#11956);
#11958=SURFACE_SIDE_STYLE('',(#11957));
#11959=SURFACE_STYLE_USAGE(.BOTH.,#11958);
#11960=PRESENTATION_STYLE_ASSIGNMENT((#11959));
ENDSEC;
END-ISO-10303-21;
